ISO-10303-21;
HEADER;
/* Generated by software containing ST-Developer
 * from STEP Tools, Inc. (www.steptools.com) 
 */

FILE_DESCRIPTION(
/* description */ (''),
/* implementation_level */ '2;1');

FILE_NAME(
/* name */ 'Pin.step',
/* time_stamp */ '2026-10-23T22:28:14+06:00',
/* author */ (''),
/* organization */ (''),
/* preprocessor_version */ 'ST-DEVELOPER v20.2',
/* originating_system */ 'Autodesk Translation Framework v15.15.0.0',
/* authorisation */ '');

FILE_SCHEMA (('AUTOMOTIVE_DESIGN { 1 0 10303 214 3 1 1 }'));
ENDSEC;

DATA;
#10=MECHANICAL_DESIGN_GEOMETRIC_PRESENTATION_REPRESENTATION('',(#104),#6753);
#74=SPHERICAL_SURFACE('',#3931,1.25);
#78=SHAPE_REPRESENTATION_RELATIONSHIP('SRR','None',#6801,#91);
#91=ADVANCED_BREP_SHAPE_REPRESENTATION('',(#117),#6741);
#104=STYLED_ITEM('',(#6921),#117);
#117=MANIFOLD_SOLID_BREP('Pin',#3753);
#131=FACE_BOUND('',#560,.T.);
#192=PLANE('',#3936);
#193=PLANE('',#3940);
#342=FACE_OUTER_BOUND('',#557,.T.);
#343=FACE_OUTER_BOUND('',#558,.T.);
#344=FACE_OUTER_BOUND('',#559,.T.);
#345=FACE_OUTER_BOUND('',#561,.T.);
#346=FACE_OUTER_BOUND('',#562,.T.);
#557=EDGE_LOOP('',(#2498,#2499,#2500));
#558=EDGE_LOOP('',(#2501,#2502,#2503,#2504));
#559=EDGE_LOOP('',(#2505));
#560=EDGE_LOOP('',(#2506));
#561=EDGE_LOOP('',(#2507,#2508,#2509,#2510));
#562=EDGE_LOOP('',(#2511));
#826=CIRCLE('',#3932,1.25);
#827=CIRCLE('',#3933,1.25);
#828=CIRCLE('',#3935,1.25);
#829=CIRCLE('',#3937,0.75);
#830=CIRCLE('',#3939,0.75);
#1043=LINE('',#5617,#1329);
#1044=LINE('',#5625,#1330);
#1329=VECTOR('',#4428,1.25);
#1330=VECTOR('',#4439,0.75);
#1618=VERTEX_POINT('',#5611);
#1619=VERTEX_POINT('',#5613);
#1620=VERTEX_POINT('',#5616);
#1621=VERTEX_POINT('',#5620);
#1622=VERTEX_POINT('',#5623);
#1966=EDGE_CURVE('',#1618,#1618,#826,.T.);
#1967=EDGE_CURVE('',#1619,#1618,#827,.T.);
#1968=EDGE_CURVE('',#1618,#1620,#1043,.T.);
#1969=EDGE_CURVE('',#1620,#1620,#828,.T.);
#1970=EDGE_CURVE('',#1621,#1621,#829,.T.);
#1971=EDGE_CURVE('',#1622,#1622,#830,.T.);
#1972=EDGE_CURVE('',#1622,#1621,#1044,.T.);
#2498=ORIENTED_EDGE('',*,*,#1966,.T.);
#2499=ORIENTED_EDGE('',*,*,#1967,.F.);
#2500=ORIENTED_EDGE('',*,*,#1967,.T.);
#2501=ORIENTED_EDGE('',*,*,#1966,.F.);
#2502=ORIENTED_EDGE('',*,*,#1968,.T.);
#2503=ORIENTED_EDGE('',*,*,#1969,.T.);
#2504=ORIENTED_EDGE('',*,*,#1968,.F.);
#2505=ORIENTED_EDGE('',*,*,#1969,.F.);
#2506=ORIENTED_EDGE('',*,*,#1970,.T.);
#2507=ORIENTED_EDGE('',*,*,#1971,.F.);
#2508=ORIENTED_EDGE('',*,*,#1972,.T.);
#2509=ORIENTED_EDGE('',*,*,#1970,.F.);
#2510=ORIENTED_EDGE('',*,*,#1972,.F.);
#2511=ORIENTED_EDGE('',*,*,#1971,.T.);
#3481=CYLINDRICAL_SURFACE('',#3934,1.25);
#3482=CYLINDRICAL_SURFACE('',#3938,0.75);
#3548=ADVANCED_FACE('',(#342),#74,.T.);
#3549=ADVANCED_FACE('',(#343),#3481,.T.);
#3550=ADVANCED_FACE('',(#344,#131),#192,.F.);
#3551=ADVANCED_FACE('',(#345),#3482,.T.);
#3552=ADVANCED_FACE('',(#346),#193,.F.);
#3753=CLOSED_SHELL('',(#3548,#3549,#3550,#3551,#3552));
#3930=AXIS2_PLACEMENT_3D('',#5609,#4418,#4419);
#3931=AXIS2_PLACEMENT_3D('',#5610,#4420,#4421);
#3932=AXIS2_PLACEMENT_3D('',#5612,#4422,#4423);
#3933=AXIS2_PLACEMENT_3D('',#5614,#4424,#4425);
#3934=AXIS2_PLACEMENT_3D('',#5615,#4426,#4427);
#3935=AXIS2_PLACEMENT_3D('',#5618,#4429,#4430);
#3936=AXIS2_PLACEMENT_3D('',#5619,#4431,#4432);
#3937=AXIS2_PLACEMENT_3D('',#5621,#4433,#4434);
#3938=AXIS2_PLACEMENT_3D('',#5622,#4435,#4436);
#3939=AXIS2_PLACEMENT_3D('',#5624,#4437,#4438);
#3940=AXIS2_PLACEMENT_3D('',#5626,#4440,#4441);
#4418=DIRECTION('axis',(0.,0.,1.));
#4419=DIRECTION('refdir',(1.,0.,0.));
#4420=DIRECTION('center_axis',(6.12323399573676E-17,0.,1.));
#4421=DIRECTION('ref_axis',(1.,0.,0.));
#4422=DIRECTION('center_axis',(0.,0.,1.));
#4423=DIRECTION('ref_axis',(1.,0.,0.));
#4424=DIRECTION('center_axis',(1.11022302462516E-16,-1.,0.));
#4425=DIRECTION('ref_axis',(-1.,-1.11022302462516E-16,0.));
#4426=DIRECTION('center_axis',(0.,0.,1.));
#4427=DIRECTION('ref_axis',(1.,0.,0.));
#4428=DIRECTION('',(0.,0.,-1.));
#4429=DIRECTION('center_axis',(0.,0.,1.));
#4430=DIRECTION('ref_axis',(1.,0.,0.));
#4431=DIRECTION('center_axis',(0.,0.,1.));
#4432=DIRECTION('ref_axis',(1.,0.,0.));
#4433=DIRECTION('center_axis',(0.,0.,1.));
#4434=DIRECTION('ref_axis',(1.,0.,0.));
#4435=DIRECTION('center_axis',(0.,0.,-1.));
#4436=DIRECTION('ref_axis',(1.,0.,0.));
#4437=DIRECTION('center_axis',(0.,0.,-1.));
#4438=DIRECTION('ref_axis',(1.,0.,0.));
#4439=DIRECTION('',(0.,0.,1.));
#4440=DIRECTION('center_axis',(0.,0.,1.));
#4441=DIRECTION('ref_axis',(1.,0.,0.));
#5609=CARTESIAN_POINT('',(0.,0.,0.));
#5610=CARTESIAN_POINT('Origin',(-2.77555756156289E-16,0.75,164.85));
#5611=CARTESIAN_POINT('',(-1.25,0.75,164.85));
#5612=CARTESIAN_POINT('Origin',(-2.77555756156289E-16,0.75,164.85));
#5613=CARTESIAN_POINT('',(-3.54096181102999E-16,0.75,166.1));
#5614=CARTESIAN_POINT('Origin',(-2.77555756156289E-16,0.75,164.85));
#5615=CARTESIAN_POINT('Origin',(-2.77555756156289E-16,0.75,150.));
#5616=CARTESIAN_POINT('',(-1.25,0.75,159.));
#5617=CARTESIAN_POINT('',(-1.25,0.75,150.));
#5618=CARTESIAN_POINT('Origin',(-2.77555756156289E-16,0.75,159.));
#5619=CARTESIAN_POINT('Origin',(-2.77555756156289E-16,0.75,159.));
#5620=CARTESIAN_POINT('',(-0.75,0.75,159.));
#5621=CARTESIAN_POINT('Origin',(-2.77555756156289E-16,0.75,159.));
#5622=CARTESIAN_POINT('Origin',(-2.77555756156289E-16,0.75,150.));
#5623=CARTESIAN_POINT('',(-0.75,0.75,144.));
#5624=CARTESIAN_POINT('Origin',(-2.77555756156289E-16,0.75,144.));
#5625=CARTESIAN_POINT('',(-0.75,0.75,150.));
#5626=CARTESIAN_POINT('Origin',(-2.77555756156289E-16,0.75,144.));
#6726=UNCERTAINTY_MEASURE_WITH_UNIT(LENGTH_MEASURE(0.01),#6754,
'DISTANCE_ACCURACY_VALUE',
'Maximum model space distance between geometric entities at asserted c
onnectivities');
#6738=UNCERTAINTY_MEASURE_WITH_UNIT(LENGTH_MEASURE(0.01),#6754,
'DISTANCE_ACCURACY_VALUE',
'Maximum model space distance between geometric entities at asserted c
onnectivities');
#6741=(
GEOMETRIC_REPRESENTATION_CONTEXT(3)
GLOBAL_UNCERTAINTY_ASSIGNED_CONTEXT((#6726))
GLOBAL_UNIT_ASSIGNED_CONTEXT((#6754,#6756,#6757))
REPRESENTATION_CONTEXT('','3D')
);
#6753=(
GEOMETRIC_REPRESENTATION_CONTEXT(3)
GLOBAL_UNCERTAINTY_ASSIGNED_CONTEXT((#6738))
GLOBAL_UNIT_ASSIGNED_CONTEXT((#6754,#6756,#6757))
REPRESENTATION_CONTEXT('','3D')
);
#6754=(
LENGTH_UNIT()
NAMED_UNIT(*)
SI_UNIT(.MILLI.,.METRE.)
);
#6756=(
NAMED_UNIT(*)
PLANE_ANGLE_UNIT()
SI_UNIT($,.RADIAN.)
);
#6757=(
NAMED_UNIT(*)
SI_UNIT($,.STERADIAN.)
SOLID_ANGLE_UNIT()
);
#6760=SHAPE_DEFINITION_REPRESENTATION(#6774,#6801);
#6774=PRODUCT_DEFINITION_SHAPE('',$,#6816);
#6801=SHAPE_REPRESENTATION('',(#3930),#6741);
#6813=PRODUCT_DEFINITION_CONTEXT('part definition',#6857,'design');
#6816=PRODUCT_DEFINITION('Pin','Pin',#6830,#6813);
#6830=PRODUCT_DEFINITION_FORMATION('',$,#6861);
#6857=APPLICATION_CONTEXT(
'Core Data for Automotive Mechanical Design Process');
#6858=PRODUCT_CONTEXT('part definition',#6857,'mechanical');
#6861=PRODUCT('Pin','Pin',$,(#6858));
#6915=COLOUR_RGB('Grey',0.48,0.52,0.57);
#6916=FILL_AREA_STYLE_COLOUR('',#6915);
#6917=FILL_AREA_STYLE('',(#6916));
#6918=SURFACE_STYLE_FILL_AREA(#6917);
#6919=SURFACE_SIDE_STYLE('',(#6918));
#6920=SURFACE_STYLE_USAGE(.BOTH.,#6919);
#6921=PRESENTATION_STYLE_ASSIGNMENT((#6920));
ENDSEC;
END-ISO-10303-21;
